ISO-10303-21;
HEADER;
/* Generated by software containing ST-Developer
 * from STEP Tools, Inc. (www.steptools.com) 
 */

FILE_DESCRIPTION(
/* description */ ('Located fixture plate with toggle clamp'),
/* implementation_level */ '2;1');

FILE_NAME(
/* name */ 'M5x14 Cap Screw.step',
/* time_stamp */ '2026-10-27T21:36:12-07:00',
/* author */ (''),
/* organization */ (''),
/* preprocessor_version */ 'ST-DEVELOPER v20.2',
/* originating_system */ 'Autodesk Translation Framework v15.17.0.0',
/* authorisation */ '');

FILE_SCHEMA (('AUTOMOTIVE_DESIGN { 1 0 10303 214 3 1 1 }'));
ENDSEC;

DATA;
#10=MECHANICAL_DESIGN_GEOMETRIC_PRESENTATION_REPRESENTATION('',(#324),#9285);
#244=ORIENTED_CLOSED_SHELL('',*,#5172,.F.);
#247=BREP_WITH_VOIDS('Body1',#5173,(#244));
#251=CONICAL_SURFACE('',#5570,0.4,0.785398163397448);
#252=CONICAL_SURFACE('',#5574,0.41,0.785398163397448);
#253=CONICAL_SURFACE('',#5578,0.26,0.463647609000806);
#276=SHAPE_REPRESENTATION_RELATIONSHIP('SRR','None',#9399,#300);
#300=ADVANCED_BREP_SHAPE_REPRESENTATION('',(#247),#9261);
#324=STYLED_ITEM('',(#9619),#247);
#387=FACE_BOUND('',#1065,.T.);
#534=PLANE('',#5558);
#535=PLANE('',#5559);
#536=PLANE('',#5560);
#537=PLANE('',#5561);
#538=PLANE('',#5562);
#539=PLANE('',#5563);
#540=PLANE('',#5564);
#541=PLANE('',#5565);
#542=PLANE('',#5566);
#543=PLANE('',#5568);
#544=PLANE('',#5576);
#735=FACE_OUTER_BOUND('',#1051,.T.);
#736=FACE_OUTER_BOUND('',#1052,.T.);
#737=FACE_OUTER_BOUND('',#1053,.T.);
#738=FACE_OUTER_BOUND('',#1054,.T.);
#739=FACE_OUTER_BOUND('',#1055,.T.);
#740=FACE_OUTER_BOUND('',#1056,.T.);
#741=FACE_OUTER_BOUND('',#1057,.T.);
#742=FACE_OUTER_BOUND('',#1058,.T.);
#743=FACE_OUTER_BOUND('',#1059,.T.);
#744=FACE_OUTER_BOUND('',#1060,.T.);
#745=FACE_OUTER_BOUND('',#1061,.T.);
#746=FACE_OUTER_BOUND('',#1062,.T.);
#747=FACE_OUTER_BOUND('',#1063,.T.);
#748=FACE_OUTER_BOUND('',#1064,.T.);
#749=FACE_OUTER_BOUND('',#1066,.T.);
#750=FACE_OUTER_BOUND('',#1067,.T.);
#1051=EDGE_LOOP('',(#3788,#3789,#3790,#3791));
#1052=EDGE_LOOP('',(#3792,#3793,#3794,#3795));
#1053=EDGE_LOOP('',(#3796,#3797,#3798,#3799));
#1054=EDGE_LOOP('',(#3800,#3801,#3802,#3803));
#1055=EDGE_LOOP('',(#3804,#3805,#3806,#3807));
#1056=EDGE_LOOP('',(#3808,#3809,#3810,#3811));
#1057=EDGE_LOOP('',(#3812,#3813,#3814,#3815,#3816,#3817));
#1058=EDGE_LOOP('',(#3818,#3819,#3820,#3821,#3822,#3823));
#1059=EDGE_LOOP('',(#3824));
#1060=EDGE_LOOP('',(#3825));
#1061=EDGE_LOOP('',(#3826,#3827,#3828,#3829));
#1062=EDGE_LOOP('',(#3830,#3831,#3832,#3833));
#1063=EDGE_LOOP('',(#3834,#3835,#3836,#3837));
#1064=EDGE_LOOP('',(#3838));
#1065=EDGE_LOOP('',(#3839));
#1066=EDGE_LOOP('',(#3840,#3841,#3842,#3843));
#1067=EDGE_LOOP('',(#3844,#3845,#3846,#3847));
#1412=CIRCLE('',#5567,0.24505);
#1413=CIRCLE('',#5569,0.375);
#1414=CIRCLE('',#5571,0.425);
#1415=CIRCLE('',#5573,0.425);
#1416=CIRCLE('',#5575,0.395);
#1417=CIRCLE('',#5577,0.27);
#1418=CIRCLE('',#5579,0.24505);
#1704=LINE('',#7899,#2114);
#1705=LINE('',#7901,#2115);
#1706=LINE('',#7903,#2116);
#1707=LINE('',#7904,#2117);
#1708=LINE('',#7907,#2118);
#1709=LINE('',#7909,#2119);
#1710=LINE('',#7910,#2120);
#1711=LINE('',#7913,#2121);
#1712=LINE('',#7915,#2122);
#1713=LINE('',#7916,#2123);
#1714=LINE('',#7919,#2124);
#1715=LINE('',#7921,#2125);
#1716=LINE('',#7922,#2126);
#1717=LINE('',#7925,#2127);
#1718=LINE('',#7927,#2128);
#1719=LINE('',#7928,#2129);
#1720=LINE('',#7930,#2130);
#1721=LINE('',#7931,#2131);
#1722=LINE('',#7943,#2132);
#1723=LINE('',#7947,#2133);
#1724=LINE('',#7951,#2134);
#1725=LINE('',#7958,#2135);
#1726=LINE('',#7960,#2136);
#2114=VECTOR('',#6348,1.);
#2115=VECTOR('',#6349,1.);
#2116=VECTOR('',#6350,1.);
#2117=VECTOR('',#6351,1.);
#2118=VECTOR('',#6354,1.);
#2119=VECTOR('',#6355,1.);
#2120=VECTOR('',#6356,1.);
#2121=VECTOR('',#6359,1.);
#2122=VECTOR('',#6360,1.);
#2123=VECTOR('',#6361,1.);
#2124=VECTOR('',#6364,1.);
#2125=VECTOR('',#6365,1.);
#2126=VECTOR('',#6366,1.);
#2127=VECTOR('',#6369,1.);
#2128=VECTOR('',#6370,1.);
#2129=VECTOR('',#6371,1.);
#2130=VECTOR('',#6374,1.);
#2131=VECTOR('',#6375,1.);
#2132=VECTOR('',#6392,0.4);
#2133=VECTOR('',#6397,0.425);
#2134=VECTOR('',#6402,0.41);
#2135=VECTOR('',#6411,0.26);
#2136=VECTOR('',#6414,0.25);
#2502=VERTEX_POINT('',#7897);
#2503=VERTEX_POINT('',#7898);
#2504=VERTEX_POINT('',#7900);
#2505=VERTEX_POINT('',#7902);
#2506=VERTEX_POINT('',#7906);
#2507=VERTEX_POINT('',#7908);
#2508=VERTEX_POINT('',#7912);
#2509=VERTEX_POINT('',#7914);
#2510=VERTEX_POINT('',#7918);
#2511=VERTEX_POINT('',#7920);
#2512=VERTEX_POINT('',#7924);
#2513=VERTEX_POINT('',#7926);
#2514=VERTEX_POINT('',#7935);
#2515=VERTEX_POINT('',#7938);
#2516=VERTEX_POINT('',#7941);
#2517=VERTEX_POINT('',#7945);
#2518=VERTEX_POINT('',#7949);
#2519=VERTEX_POINT('',#7953);
#2520=VERTEX_POINT('',#7956);
#2982=EDGE_CURVE('',#2502,#2503,#1704,.T.);
#2983=EDGE_CURVE('',#2503,#2504,#1705,.T.);
#2984=EDGE_CURVE('',#2504,#2505,#1706,.T.);
#2985=EDGE_CURVE('',#2502,#2505,#1707,.T.);
#2986=EDGE_CURVE('',#2503,#2506,#1708,.T.);
#2987=EDGE_CURVE('',#2506,#2507,#1709,.T.);
#2988=EDGE_CURVE('',#2507,#2504,#1710,.T.);
#2989=EDGE_CURVE('',#2506,#2508,#1711,.T.);
#2990=EDGE_CURVE('',#2508,#2509,#1712,.T.);
#2991=EDGE_CURVE('',#2509,#2507,#1713,.T.);
#2992=EDGE_CURVE('',#2508,#2510,#1714,.T.);
#2993=EDGE_CURVE('',#2510,#2511,#1715,.T.);
#2994=EDGE_CURVE('',#2511,#2509,#1716,.T.);
#2995=EDGE_CURVE('',#2510,#2512,#1717,.T.);
#2996=EDGE_CURVE('',#2512,#2513,#1718,.T.);
#2997=EDGE_CURVE('',#2513,#2511,#1719,.T.);
#2998=EDGE_CURVE('',#2512,#2502,#1720,.T.);
#2999=EDGE_CURVE('',#2505,#2513,#1721,.T.);
#3000=EDGE_CURVE('',#2514,#2514,#1412,.T.);
#3001=EDGE_CURVE('',#2515,#2515,#1413,.T.);
#3002=EDGE_CURVE('',#2516,#2516,#1414,.T.);
#3003=EDGE_CURVE('',#2516,#2515,#1722,.T.);
#3004=EDGE_CURVE('',#2517,#2517,#1415,.T.);
#3005=EDGE_CURVE('',#2517,#2516,#1723,.T.);
#3006=EDGE_CURVE('',#2518,#2518,#1416,.T.);
#3007=EDGE_CURVE('',#2518,#2517,#1724,.T.);
#3008=EDGE_CURVE('',#2519,#2519,#1417,.T.);
#3009=EDGE_CURVE('',#2520,#2520,#1418,.F.);
#3010=EDGE_CURVE('',#2520,#2519,#1725,.T.);
#3011=EDGE_CURVE('',#2514,#2520,#1726,.T.);
#3788=ORIENTED_EDGE('',*,*,#2982,.T.);
#3789=ORIENTED_EDGE('',*,*,#2983,.T.);
#3790=ORIENTED_EDGE('',*,*,#2984,.T.);
#3791=ORIENTED_EDGE('',*,*,#2985,.F.);
#3792=ORIENTED_EDGE('',*,*,#2986,.T.);
#3793=ORIENTED_EDGE('',*,*,#2987,.T.);
#3794=ORIENTED_EDGE('',*,*,#2988,.T.);
#3795=ORIENTED_EDGE('',*,*,#2983,.F.);
#3796=ORIENTED_EDGE('',*,*,#2989,.T.);
#3797=ORIENTED_EDGE('',*,*,#2990,.T.);
#3798=ORIENTED_EDGE('',*,*,#2991,.T.);
#3799=ORIENTED_EDGE('',*,*,#2987,.F.);
#3800=ORIENTED_EDGE('',*,*,#2992,.T.);
#3801=ORIENTED_EDGE('',*,*,#2993,.T.);
#3802=ORIENTED_EDGE('',*,*,#2994,.T.);
#3803=ORIENTED_EDGE('',*,*,#2990,.F.);
#3804=ORIENTED_EDGE('',*,*,#2995,.T.);
#3805=ORIENTED_EDGE('',*,*,#2996,.T.);
#3806=ORIENTED_EDGE('',*,*,#2997,.T.);
#3807=ORIENTED_EDGE('',*,*,#2993,.F.);
#3808=ORIENTED_EDGE('',*,*,#2998,.T.);
#3809=ORIENTED_EDGE('',*,*,#2985,.T.);
#3810=ORIENTED_EDGE('',*,*,#2999,.T.);
#3811=ORIENTED_EDGE('',*,*,#2996,.F.);
#3812=ORIENTED_EDGE('',*,*,#2998,.F.);
#3813=ORIENTED_EDGE('',*,*,#2995,.F.);
#3814=ORIENTED_EDGE('',*,*,#2992,.F.);
#3815=ORIENTED_EDGE('',*,*,#2989,.F.);
#3816=ORIENTED_EDGE('',*,*,#2986,.F.);
#3817=ORIENTED_EDGE('',*,*,#2982,.F.);
#3818=ORIENTED_EDGE('',*,*,#2999,.F.);
#3819=ORIENTED_EDGE('',*,*,#2984,.F.);
#3820=ORIENTED_EDGE('',*,*,#2988,.F.);
#3821=ORIENTED_EDGE('',*,*,#2991,.F.);
#3822=ORIENTED_EDGE('',*,*,#2994,.F.);
#3823=ORIENTED_EDGE('',*,*,#2997,.F.);
#3824=ORIENTED_EDGE('',*,*,#3000,.F.);
#3825=ORIENTED_EDGE('',*,*,#3001,.F.);
#3826=ORIENTED_EDGE('',*,*,#3002,.F.);
#3827=ORIENTED_EDGE('',*,*,#3003,.T.);
#3828=ORIENTED_EDGE('',*,*,#3001,.T.);
#3829=ORIENTED_EDGE('',*,*,#3003,.F.);
#3830=ORIENTED_EDGE('',*,*,#3004,.F.);
#3831=ORIENTED_EDGE('',*,*,#3005,.T.);
#3832=ORIENTED_EDGE('',*,*,#3002,.T.);
#3833=ORIENTED_EDGE('',*,*,#3005,.F.);
#3834=ORIENTED_EDGE('',*,*,#3006,.F.);
#3835=ORIENTED_EDGE('',*,*,#3007,.T.);
#3836=ORIENTED_EDGE('',*,*,#3004,.T.);
#3837=ORIENTED_EDGE('',*,*,#3007,.F.);
#3838=ORIENTED_EDGE('',*,*,#3006,.T.);
#3839=ORIENTED_EDGE('',*,*,#3008,.F.);
#3840=ORIENTED_EDGE('',*,*,#3009,.F.);
#3841=ORIENTED_EDGE('',*,*,#3010,.T.);
#3842=ORIENTED_EDGE('',*,*,#3008,.T.);
#3843=ORIENTED_EDGE('',*,*,#3010,.F.);
#3844=ORIENTED_EDGE('',*,*,#3000,.T.);
#3845=ORIENTED_EDGE('',*,*,#3011,.T.);
#3846=ORIENTED_EDGE('',*,*,#3009,.T.);
#3847=ORIENTED_EDGE('',*,*,#3011,.F.);
#4805=CYLINDRICAL_SURFACE('',#5572,0.425);
#4806=CYLINDRICAL_SURFACE('',#5580,0.24505);
#4936=ADVANCED_FACE('',(#735),#534,.F.);
#4937=ADVANCED_FACE('',(#736),#535,.F.);
#4938=ADVANCED_FACE('',(#737),#536,.F.);
#4939=ADVANCED_FACE('',(#738),#537,.F.);
#4940=ADVANCED_FACE('',(#739),#538,.F.);
#4941=ADVANCED_FACE('',(#740),#539,.F.);
#4942=ADVANCED_FACE('',(#741),#540,.F.);
#4943=ADVANCED_FACE('',(#742),#541,.F.);
#4944=ADVANCED_FACE('',(#743),#542,.F.);
#4945=ADVANCED_FACE('',(#744),#543,.T.);
#4946=ADVANCED_FACE('',(#745),#251,.T.);
#4947=ADVANCED_FACE('',(#746),#4805,.T.);
#4948=ADVANCED_FACE('',(#747),#252,.T.);
#4949=ADVANCED_FACE('',(#748,#387),#544,.T.);
#4950=ADVANCED_FACE('',(#749),#253,.T.);
#4951=ADVANCED_FACE('',(#750),#4806,.T.);
#5172=CLOSED_SHELL('',(#4936,#4937,#4938,#4939,#4940,#4941,#4942,#4943));
#5173=CLOSED_SHELL('',(#4944,#4945,#4946,#4947,#4948,#4949,#4950,#4951));
#5557=AXIS2_PLACEMENT_3D('',#7895,#6344,#6345);
#5558=AXIS2_PLACEMENT_3D('',#7896,#6346,#6347);
#5559=AXIS2_PLACEMENT_3D('',#7905,#6352,#6353);
#5560=AXIS2_PLACEMENT_3D('',#7911,#6357,#6358);
#5561=AXIS2_PLACEMENT_3D('',#7917,#6362,#6363);
#5562=AXIS2_PLACEMENT_3D('',#7923,#6367,#6368);
#5563=AXIS2_PLACEMENT_3D('',#7929,#6372,#6373);
#5564=AXIS2_PLACEMENT_3D('',#7932,#6376,#6377);
#5565=AXIS2_PLACEMENT_3D('',#7933,#6378,#6379);
#5566=AXIS2_PLACEMENT_3D('',#7934,#6380,#6381);
#5567=AXIS2_PLACEMENT_3D('',#7936,#6382,#6383);
#5568=AXIS2_PLACEMENT_3D('',#7937,#6384,#6385);
#5569=AXIS2_PLACEMENT_3D('',#7939,#6386,#6387);
#5570=AXIS2_PLACEMENT_3D('',#7940,#6388,#6389);
#5571=AXIS2_PLACEMENT_3D('',#7942,#6390,#6391);
#5572=AXIS2_PLACEMENT_3D('',#7944,#6393,#6394);
#5573=AXIS2_PLACEMENT_3D('',#7946,#6395,#6396);
#5574=AXIS2_PLACEMENT_3D('',#7948,#6398,#6399);
#5575=AXIS2_PLACEMENT_3D('',#7950,#6400,#6401);
#5576=AXIS2_PLACEMENT_3D('',#7952,#6403,#6404);
#5577=AXIS2_PLACEMENT_3D('',#7954,#6405,#6406);
#5578=AXIS2_PLACEMENT_3D('',#7955,#6407,#6408);
#5579=AXIS2_PLACEMENT_3D('',#7957,#6409,#6410);
#5580=AXIS2_PLACEMENT_3D('',#7959,#6412,#6413);
#6344=DIRECTION('axis',(0.,0.,1.));
#6345=DIRECTION('refdir',(1.,0.,0.));
#6346=DIRECTION('center_axis',(0.866025403784439,0.,-0.5));
#6347=DIRECTION('ref_axis',(0.5,0.,0.866025403784439));
#6348=DIRECTION('',(-0.5,0.,-0.866025403784439));
#6349=DIRECTION('',(0.,-1.,0.));
#6350=DIRECTION('',(0.5,0.,0.866025403784439));
#6351=DIRECTION('',(0.,-1.,0.));
#6352=DIRECTION('center_axis',(1.20185167898973E-16,0.,-1.));
#6353=DIRECTION('ref_axis',(1.,0.,1.20185167898973E-16));
#6354=DIRECTION('',(-1.,0.,-1.20185167898973E-16));
#6355=DIRECTION('',(0.,-1.,0.));
#6356=DIRECTION('',(1.,0.,1.20185167898973E-16));
#6357=DIRECTION('center_axis',(-0.866025403784439,0.,-0.5));
#6358=DIRECTION('ref_axis',(0.5,0.,-0.866025403784439));
#6359=DIRECTION('',(-0.5,0.,0.866025403784439));
#6360=DIRECTION('',(0.,-1.,0.));
#6361=DIRECTION('',(0.5,0.,-0.866025403784439));
#6362=DIRECTION('center_axis',(-0.866025403784439,0.,0.5));
#6363=DIRECTION('ref_axis',(-0.5,0.,-0.866025403784439));
#6364=DIRECTION('',(0.5,0.,0.866025403784439));
#6365=DIRECTION('',(0.,-1.,0.));
#6366=DIRECTION('',(-0.5,0.,-0.866025403784439));
#6367=DIRECTION('center_axis',(-2.40370335797945E-16,0.,1.));
#6368=DIRECTION('ref_axis',(-1.,0.,-2.40370335797945E-16));
#6369=DIRECTION('',(1.,0.,2.40370335797945E-16));
#6370=DIRECTION('',(0.,-1.,0.));
#6371=DIRECTION('',(-1.,0.,-2.40370335797945E-16));
#6372=DIRECTION('center_axis',(0.866025403784439,0.,0.5));
#6373=DIRECTION('ref_axis',(-0.5,0.,0.866025403784439));
#6374=DIRECTION('',(0.5,0.,-0.866025403784439));
#6375=DIRECTION('',(-0.5,0.,0.866025403784439));
#6376=DIRECTION('center_axis',(0.,1.,0.));
#6377=DIRECTION('ref_axis',(1.,0.,0.));
#6378=DIRECTION('center_axis',(0.,-1.,0.));
#6379=DIRECTION('ref_axis',(0.,0.,-1.));
#6380=DIRECTION('center_axis',(0.,1.,0.));
#6381=DIRECTION('ref_axis',(1.,0.,0.));
#6382=DIRECTION('center_axis',(0.,1.,0.));
#6383=DIRECTION('ref_axis',(1.,0.,0.));
#6384=DIRECTION('center_axis',(0.,1.,0.));
#6385=DIRECTION('ref_axis',(0.,0.,1.));
#6386=DIRECTION('center_axis',(0.,-1.,0.));
#6387=DIRECTION('ref_axis',(1.,0.,0.));
#6388=DIRECTION('center_axis',(0.,-1.,0.));
#6389=DIRECTION('ref_axis',(1.,0.,0.));
#6390=DIRECTION('center_axis',(0.,-1.,0.));
#6391=DIRECTION('ref_axis',(1.,0.,0.));
#6392=DIRECTION('',(0.707106781186548,0.707106781186547,8.65956056235493E-17));
#6393=DIRECTION('center_axis',(0.,-1.,0.));
#6394=DIRECTION('ref_axis',(1.,0.,0.));
#6395=DIRECTION('center_axis',(0.,-1.,0.));
#6396=DIRECTION('ref_axis',(1.,0.,0.));
#6397=DIRECTION('',(0.,1.,0.));
#6398=DIRECTION('center_axis',(0.,1.,0.));
#6399=DIRECTION('ref_axis',(1.,0.,0.));
#6400=DIRECTION('center_axis',(0.,-1.,0.));
#6401=DIRECTION('ref_axis',(1.,0.,0.));
#6402=DIRECTION('',(-0.707106781186547,0.707106781186548,-8.65956056235493E-17));
#6403=DIRECTION('center_axis',(0.,-1.,0.));
#6404=DIRECTION('ref_axis',(0.,0.,-1.));
#6405=DIRECTION('center_axis',(0.,-1.,0.));
#6406=DIRECTION('ref_axis',(1.,0.,0.));
#6407=DIRECTION('center_axis',(0.,1.,0.));
#6408=DIRECTION('ref_axis',(1.,0.,0.));
#6409=DIRECTION('center_axis',(0.,1.,0.));
#6410=DIRECTION('ref_axis',(1.,0.,0.));
#6411=DIRECTION('',(-0.447213595499958,0.894427190999916,-5.47678698264203E-17));
#6412=DIRECTION('center_axis',(0.,-1.,0.));
#6413=DIRECTION('ref_axis',(1.,0.,0.));
#6414=DIRECTION('',(0.,1.,0.));
#7895=CARTESIAN_POINT('',(0.,0.,0.));
#7896=CARTESIAN_POINT('Origin',(0.115470053837925,-0.5,-0.2));
#7897=CARTESIAN_POINT('',(0.23094010767585,-0.5,0.));
#7898=CARTESIAN_POINT('',(0.115470053837925,-0.5,-0.2));
#7899=CARTESIAN_POINT('',(0.23094010767585,-0.5,0.));
#7900=CARTESIAN_POINT('',(0.115470053837925,-0.8,-0.2));
#7901=CARTESIAN_POINT('',(0.115470053837925,-0.5,-0.2));
#7902=CARTESIAN_POINT('',(0.23094010767585,-0.8,0.));
#7903=CARTESIAN_POINT('',(0.23094010767585,-0.8,0.));
#7904=CARTESIAN_POINT('',(0.23094010767585,-0.5,0.));
#7905=CARTESIAN_POINT('Origin',(-0.115470053837925,-0.5,-0.2));
#7906=CARTESIAN_POINT('',(-0.115470053837925,-0.5,-0.2));
#7907=CARTESIAN_POINT('',(0.115470053837925,-0.5,-0.2));
#7908=CARTESIAN_POINT('',(-0.115470053837925,-0.8,-0.2));
#7909=CARTESIAN_POINT('',(-0.115470053837925,-0.5,-0.2));
#7910=CARTESIAN_POINT('',(0.115470053837925,-0.8,-0.2));
#7911=CARTESIAN_POINT('Origin',(-0.23094010767585,-0.5,-2.77555756156289E-17));
#7912=CARTESIAN_POINT('',(-0.23094010767585,-0.5,-2.82820063659975E-17));
#7913=CARTESIAN_POINT('',(-0.115470053837925,-0.5,-0.2));
#7914=CARTESIAN_POINT('',(-0.23094010767585,-0.8,-2.77555756156289E-17));
#7915=CARTESIAN_POINT('',(-0.23094010767585,-0.5,-2.82820063659975E-17));
#7916=CARTESIAN_POINT('',(-0.115470053837925,-0.8,-0.2));
#7917=CARTESIAN_POINT('Origin',(-0.115470053837925,-0.5,0.2));
#7918=CARTESIAN_POINT('',(-0.115470053837925,-0.5,0.2));
#7919=CARTESIAN_POINT('',(-0.23094010767585,-0.5,-2.82820063659975E-17));
#7920=CARTESIAN_POINT('',(-0.115470053837925,-0.8,0.2));
#7921=CARTESIAN_POINT('',(-0.115470053837925,-0.5,0.2));
#7922=CARTESIAN_POINT('',(-0.23094010767585,-0.8,-2.82820063659975E-17));
#7923=CARTESIAN_POINT('Origin',(0.115470053837925,-0.5,0.2));
#7924=CARTESIAN_POINT('',(0.115470053837925,-0.5,0.2));
#7925=CARTESIAN_POINT('',(-0.115470053837925,-0.5,0.2));
#7926=CARTESIAN_POINT('',(0.115470053837925,-0.8,0.2));
#7927=CARTESIAN_POINT('',(0.115470053837925,-0.5,0.2));
#7928=CARTESIAN_POINT('',(-0.115470053837925,-0.8,0.2));
#7929=CARTESIAN_POINT('Origin',(0.23094010767585,-0.5,0.));
#7930=CARTESIAN_POINT('',(0.115470053837925,-0.5,0.2));
#7931=CARTESIAN_POINT('',(0.115470053837925,-0.8,0.2));
#7932=CARTESIAN_POINT('Origin',(0.,-0.5,0.));
#7933=CARTESIAN_POINT('Origin',(0.,-0.8,0.));
#7934=CARTESIAN_POINT('Origin',(0.,-1.4,0.));
#7935=CARTESIAN_POINT('',(-0.24505,-1.4,3.00099698131059E-17));
#7936=CARTESIAN_POINT('Origin',(0.,-1.4,0.));
#7937=CARTESIAN_POINT('Origin',(0.375,0.5,0.));
#7938=CARTESIAN_POINT('',(-0.375,0.5,-4.59242549680257E-17));
#7939=CARTESIAN_POINT('Origin',(0.,0.5,0.));
#7940=CARTESIAN_POINT('Origin',(0.,0.475,0.));
#7941=CARTESIAN_POINT('',(-0.425,0.45,-5.20474889637625E-17));
#7942=CARTESIAN_POINT('Origin',(0.,0.45,0.));
#7943=CARTESIAN_POINT('',(-0.4,0.475,-4.89858719658941E-17));
#7944=CARTESIAN_POINT('Origin',(0.,0.24,0.));
#7945=CARTESIAN_POINT('',(-0.425,0.0299999999999998,-5.20474889637625E-17));
#7946=CARTESIAN_POINT('Origin',(0.,0.0299999999999998,0.));
#7947=CARTESIAN_POINT('',(-0.425,0.24,-5.20474889637625E-17));
#7948=CARTESIAN_POINT('Origin',(0.,0.0150000000000001,0.));
#7949=CARTESIAN_POINT('',(-0.395,4.85722573273506E-17,-4.83735485663204E-17));
#7950=CARTESIAN_POINT('Origin',(0.,0.,0.));
#7951=CARTESIAN_POINT('',(-0.41,0.0150000000000001,-5.02105187650415E-17));
#7952=CARTESIAN_POINT('Origin',(0.27,0.,0.));
#7953=CARTESIAN_POINT('',(-0.27,0.,-3.30654635769785E-17));
#7954=CARTESIAN_POINT('Origin',(0.,0.,0.));
#7955=CARTESIAN_POINT('Origin',(0.,-0.02,0.));
#7956=CARTESIAN_POINT('',(-0.24505,-0.0498999999999999,3.00099698131059E-17));
#7957=CARTESIAN_POINT('Origin',(0.,-0.0498999999999999,0.));
#7958=CARTESIAN_POINT('',(-0.26,-0.02,-3.18408167778312E-17));
#7959=CARTESIAN_POINT('Origin',(0.,-0.995,0.));
#7960=CARTESIAN_POINT('',(-0.24505,-0.995,-3.00099698131059E-17));
#9231=UNCERTAINTY_MEASURE_WITH_UNIT(LENGTH_MEASURE(0.001),#9286,
'DISTANCE_ACCURACY_VALUE',
'Maximum model space distance between geometric entities at asserted c
onnectivities');
#9255=UNCERTAINTY_MEASURE_WITH_UNIT(LENGTH_MEASURE(0.001),#9286,
'DISTANCE_ACCURACY_VALUE',
'Maximum model space distance between geometric entities at asserted c
onnectivities');
#9261=(
GEOMETRIC_REPRESENTATION_CONTEXT(3)
GLOBAL_UNCERTAINTY_ASSIGNED_CONTEXT((#9231))
GLOBAL_UNIT_ASSIGNED_CONTEXT((#9286,#9288,#9289))
REPRESENTATION_CONTEXT('','3D')
);
#9285=(
GEOMETRIC_REPRESENTATION_CONTEXT(3)
GLOBAL_UNCERTAINTY_ASSIGNED_CONTEXT((#9255))
GLOBAL_UNIT_ASSIGNED_CONTEXT((#9286,#9288,#9289))
REPRESENTATION_CONTEXT('','3D')
);
#9286=(
LENGTH_UNIT()
NAMED_UNIT(*)
SI_UNIT(.CENTI.,.METRE.)
);
#9288=(
NAMED_UNIT(*)
PLANE_ANGLE_UNIT()
SI_UNIT($,.RADIAN.)
);
#9289=(
NAMED_UNIT(*)
SI_UNIT($,.STERADIAN.)
SOLID_ANGLE_UNIT()
);
#9295=SHAPE_DEFINITION_REPRESENTATION(#9324,#9399);
#9324=PRODUCT_DEFINITION_SHAPE('',$,#9429);
#9399=SHAPE_REPRESENTATION('',(#5557),#9261);
#9423=PRODUCT_DEFINITION_CONTEXT('part definition',#9512,'design');
#9429=PRODUCT_DEFINITION('M5x14 Cap Screw','M5x14 Cap Screw',#9458,#9423);
#9458=PRODUCT_DEFINITION_FORMATION('',$,#9519);
#9512=APPLICATION_CONTEXT(
'Core Data for Automotive Mechanical Design Process');
#9513=PRODUCT_CONTEXT('part definition',#9512,'mechanical');
#9519=PRODUCT('M5x14 Cap Screw','M5x14 Cap Screw','M5x14 Cap Screw',(#9513));
#9613=COLOUR_RGB('Black',0.12,0.14,0.17);
#9614=FILL_AREA_STYLE_COLOUR('',#9613);
#9615=FILL_AREA_STYLE('',(#9614));
#9616=SURFACE_STYLE_FILL_AREA(#9615);
#9617=SURFACE_SIDE_STYLE('',(#9616));
#9618=SURFACE_STYLE_USAGE(.BOTH.,#9617);
#9619=PRESENTATION_STYLE_ASSIGNMENT((#9618));
ENDSEC;
END-ISO-10303-21;
